ISO-10303-21;
HEADER;
/* Generated by software containing ST-Developer
 * from STEP Tools, Inc. (www.steptools.com) 
 */

FILE_DESCRIPTION(
/* description */ ('Counterbalanced vertical column'),
/* implementation_level */ '2;1');

FILE_NAME(
/* name */ 'Lock screw and knob.step',
/* time_stamp */ '2026-10-29T16:47:22-07:00',
/* author */ (''),
/* organization */ (''),
/* preprocessor_version */ 'ST-DEVELOPER v20.2',
/* originating_system */ 'Autodesk Translation Framework v15.17.0.0',
/* authorisation */ '');

FILE_SCHEMA (('AUTOMOTIVE_DESIGN { 1 0 10303 214 3 1 1 }'));
ENDSEC;

DATA;
#10=MECHANICAL_DESIGN_GEOMETRIC_PRESENTATION_REPRESENTATION('',(#379),#15040);
#309=SHAPE_REPRESENTATION_RELATIONSHIP('SRR','None',#15214,#344);
#344=ADVANCED_BREP_SHAPE_REPRESENTATION('',(#412),#15033);
#379=STYLED_ITEM('',(#15464),#412);
#412=MANIFOLD_SOLID_BREP('Body1',#7104);
#524=FACE_BOUND('',#1667,.T.);
#763=PLANE('',#8044);
#764=PLANE('',#8045);
#765=PLANE('',#8049);
#1151=FACE_OUTER_BOUND('',#1664,.T.);
#1152=FACE_OUTER_BOUND('',#1665,.T.);
#1153=FACE_OUTER_BOUND('',#1666,.T.);
#1154=FACE_OUTER_BOUND('',#1668,.T.);
#1155=FACE_OUTER_BOUND('',#1669,.T.);
#1664=EDGE_LOOP('',(#6198,#6199,#6200,#6201));
#1665=EDGE_LOOP('',(#6202));
#1666=EDGE_LOOP('',(#6203));
#1667=EDGE_LOOP('',(#6204));
#1668=EDGE_LOOP('',(#6205,#6206,#6207,#6208));
#1669=EDGE_LOOP('',(#6209));
#2269=LINE('',#14509,#2940);
#2270=LINE('',#14517,#2941);
#2940=VECTOR('',#9829,1.2);
#2941=VECTOR('',#9840,0.3);
#3271=CIRCLE('',#8042,1.2);
#3272=CIRCLE('',#8043,1.2);
#3273=CIRCLE('',#8046,0.3);
#3274=CIRCLE('',#8048,0.3);
#3772=VERTEX_POINT('',#14506);
#3773=VERTEX_POINT('',#14508);
#3774=VERTEX_POINT('',#14513);
#3775=VERTEX_POINT('',#14516);
#4600=EDGE_CURVE('',#3772,#3772,#3271,.T.);
#4601=EDGE_CURVE('',#3772,#3773,#2269,.T.);
#4602=EDGE_CURVE('',#3773,#3773,#3272,.T.);
#4603=EDGE_CURVE('',#3774,#3774,#3273,.T.);
#4604=EDGE_CURVE('',#3774,#3775,#2270,.T.);
#4605=EDGE_CURVE('',#3775,#3775,#3274,.T.);
#6198=ORIENTED_EDGE('',*,*,#4600,.F.);
#6199=ORIENTED_EDGE('',*,*,#4601,.T.);
#6200=ORIENTED_EDGE('',*,*,#4602,.T.);
#6201=ORIENTED_EDGE('',*,*,#4601,.F.);
#6202=ORIENTED_EDGE('',*,*,#4600,.T.);
#6203=ORIENTED_EDGE('',*,*,#4602,.F.);
#6204=ORIENTED_EDGE('',*,*,#4603,.F.);
#6205=ORIENTED_EDGE('',*,*,#4603,.T.);
#6206=ORIENTED_EDGE('',*,*,#4604,.T.);
#6207=ORIENTED_EDGE('',*,*,#4605,.T.);
#6208=ORIENTED_EDGE('',*,*,#4604,.F.);
#6209=ORIENTED_EDGE('',*,*,#4605,.F.);
#6658=CYLINDRICAL_SURFACE('',#8041,1.2);
#6659=CYLINDRICAL_SURFACE('',#8047,0.3);
#6993=ADVANCED_FACE('',(#1151),#6658,.T.);
#6994=ADVANCED_FACE('',(#1152),#763,.T.);
#6995=ADVANCED_FACE('',(#1153,#524),#764,.F.);
#6996=ADVANCED_FACE('',(#1154),#6659,.T.);
#6997=ADVANCED_FACE('',(#1155),#765,.F.);
#7104=CLOSED_SHELL('',(#6993,#6994,#6995,#6996,#6997));
#8040=AXIS2_PLACEMENT_3D('',#14504,#9823,#9824);
#8041=AXIS2_PLACEMENT_3D('',#14505,#9825,#9826);
#8042=AXIS2_PLACEMENT_3D('',#14507,#9827,#9828);
#8043=AXIS2_PLACEMENT_3D('',#14510,#9830,#9831);
#8044=AXIS2_PLACEMENT_3D('',#14511,#9832,#9833);
#8045=AXIS2_PLACEMENT_3D('',#14512,#9834,#9835);
#8046=AXIS2_PLACEMENT_3D('',#14514,#9836,#9837);
#8047=AXIS2_PLACEMENT_3D('',#14515,#9838,#9839);
#8048=AXIS2_PLACEMENT_3D('',#14518,#9841,#9842);
#8049=AXIS2_PLACEMENT_3D('',#14519,#9843,#9844);
#9823=DIRECTION('axis',(0.,0.,1.));
#9824=DIRECTION('refdir',(1.,0.,0.));
#9825=DIRECTION('center_axis',(0.,1.,0.));
#9826=DIRECTION('ref_axis',(1.,0.,0.));
#9827=DIRECTION('center_axis',(0.,1.,0.));
#9828=DIRECTION('ref_axis',(1.,0.,0.));
#9829=DIRECTION('',(0.,-1.,0.));
#9830=DIRECTION('center_axis',(0.,1.,0.));
#9831=DIRECTION('ref_axis',(1.,0.,0.));
#9832=DIRECTION('center_axis',(0.,1.,0.));
#9833=DIRECTION('ref_axis',(1.,0.,0.));
#9834=DIRECTION('center_axis',(0.,1.,0.));
#9835=DIRECTION('ref_axis',(1.,0.,0.));
#9836=DIRECTION('center_axis',(0.,-1.,0.));
#9837=DIRECTION('ref_axis',(1.,0.,0.));
#9838=DIRECTION('center_axis',(0.,1.,0.));
#9839=DIRECTION('ref_axis',(1.,0.,0.));
#9840=DIRECTION('',(0.,-1.,0.));
#9841=DIRECTION('center_axis',(0.,1.,0.));
#9842=DIRECTION('ref_axis',(1.,0.,0.));
#9843=DIRECTION('center_axis',(0.,1.,0.));
#9844=DIRECTION('ref_axis',(1.,0.,0.));
#14504=CARTESIAN_POINT('',(0.,0.,0.));
#14505=CARTESIAN_POINT('Origin',(1.8,3.6,17.6));
#14506=CARTESIAN_POINT('',(0.6,4.4,17.6));
#14507=CARTESIAN_POINT('Origin',(1.8,4.4,17.6));
#14508=CARTESIAN_POINT('',(0.6,3.6,17.6));
#14509=CARTESIAN_POINT('',(0.6,3.6,17.6));
#14510=CARTESIAN_POINT('Origin',(1.8,3.6,17.6));
#14511=CARTESIAN_POINT('Origin',(1.8,4.4,17.6));
#14512=CARTESIAN_POINT('Origin',(1.8,3.6,17.6));
#14513=CARTESIAN_POINT('',(1.5,3.6,17.6));
#14514=CARTESIAN_POINT('Origin',(1.8,3.6,17.6));
#14515=CARTESIAN_POINT('Origin',(1.8,1.8,17.6));
#14516=CARTESIAN_POINT('',(1.5,1.8,17.6));
#14517=CARTESIAN_POINT('',(1.5,1.8,17.6));
#14518=CARTESIAN_POINT('Origin',(1.8,1.8,17.6));
#14519=CARTESIAN_POINT('Origin',(1.8,1.8,17.6));
#14993=UNCERTAINTY_MEASURE_WITH_UNIT(LENGTH_MEASURE(0.001),#15041,
'DISTANCE_ACCURACY_VALUE',
'Maximum model space distance between geometric entities at asserted c
onnectivities');
#15000=UNCERTAINTY_MEASURE_WITH_UNIT(LENGTH_MEASURE(0.001),#15041,
'DISTANCE_ACCURACY_VALUE',
'Maximum model space distance between geometric entities at asserted c
onnectivities');
#15033=(
GEOMETRIC_REPRESENTATION_CONTEXT(3)
GLOBAL_UNCERTAINTY_ASSIGNED_CONTEXT((#14993))
GLOBAL_UNIT_ASSIGNED_CONTEXT((#15041,#15043,#15044))
REPRESENTATION_CONTEXT('','3D')
);
#15040=(
GEOMETRIC_REPRESENTATION_CONTEXT(3)
GLOBAL_UNCERTAINTY_ASSIGNED_CONTEXT((#15000))
GLOBAL_UNIT_ASSIGNED_CONTEXT((#15041,#15043,#15044))
REPRESENTATION_CONTEXT('','3D')
);
#15041=(
LENGTH_UNIT()
NAMED_UNIT(*)
SI_UNIT(.CENTI.,.METRE.)
);
#15043=(
NAMED_UNIT(*)
PLANE_ANGLE_UNIT()
SI_UNIT($,.RADIAN.)
);
#15044=(
NAMED_UNIT(*)
SI_UNIT($,.STERADIAN.)
SOLID_ANGLE_UNIT()
);
#15077=SHAPE_DEFINITION_REPRESENTATION(#15116,#15214);
#15116=PRODUCT_DEFINITION_SHAPE('',$,#15254);
#15214=SHAPE_REPRESENTATION('',(#8040),#15033);
#15221=PRODUCT_DEFINITION_CONTEXT('part definition',#15340,'design');
#15254=PRODUCT_DEFINITION('Lock screw and knob','Lock screw and knob',#15293,
#15221);
#15293=PRODUCT_DEFINITION_FORMATION('',$,#15374);
#15340=APPLICATION_CONTEXT(
'Core Data for Automotive Mechanical Design Process');
#15341=PRODUCT_CONTEXT('part definition',#15340,'mechanical');
#15374=PRODUCT('Lock screw and knob','Lock screw and knob',
'Lock screw and knob',(#15341));
#15458=COLOUR_RGB('Black',0.12,0.14,0.17);
#15459=FILL_AREA_STYLE_COLOUR('',#15458);
#15460=FILL_AREA_STYLE('',(#15459));
#15461=SURFACE_STYLE_FILL_AREA(#15460);
#15462=SURFACE_SIDE_STYLE('',(#15461));
#15463=SURFACE_STYLE_USAGE(.BOTH.,#15462);
#15464=PRESENTATION_STYLE_ASSIGNMENT((#15463));
ENDSEC;
END-ISO-10303-21;
